ISO-10303-21;
HEADER;
/* Generated by software containing ST-Developer
 * from STEP Tools, Inc. (www.steptools.com) 
 */

FILE_DESCRIPTION(
/* description */ ('Turntable on roller ring'),
/* implementation_level */ '2;1');

FILE_NAME(
/* name */ 'Inner race spacer (3).step',
/* time_stamp */ '2026-10-28T03:23:59-07:00',
/* author */ (''),
/* organization */ (''),
/* preprocessor_version */ 'ST-DEVELOPER v20.2',
/* originating_system */ 'Autodesk Translation Framework v15.17.0.0',
/* authorisation */ '');

FILE_SCHEMA (('AUTOMOTIVE_DESIGN { 1 0 10303 214 3 1 1 }'));
ENDSEC;

DATA;
#10=MECHANICAL_DESIGN_GEOMETRIC_PRESENTATION_REPRESENTATION('',(#650),#16281);
#531=SHAPE_REPRESENTATION_RELATIONSHIP('SRR','None',#16549,#586);
#586=ADVANCED_BREP_SHAPE_REPRESENTATION('',(#720),#16243);
#650=STYLED_ITEM('',(#16932),#720);
#720=MANIFOLD_SOLID_BREP('Body1',#8393);
#907=FACE_BOUND('',#2192,.T.);
#908=FACE_BOUND('',#2194,.T.);
#1131=PLANE('',#9675);
#1132=PLANE('',#9676);
#1534=FACE_OUTER_BOUND('',#2189,.T.);
#1535=FACE_OUTER_BOUND('',#2190,.T.);
#1536=FACE_OUTER_BOUND('',#2191,.T.);
#1537=FACE_OUTER_BOUND('',#2193,.T.);
#2189=EDGE_LOOP('',(#6845,#6846,#6847,#6848));
#2190=EDGE_LOOP('',(#6849,#6850,#6851,#6852));
#2191=EDGE_LOOP('',(#6853));
#2192=EDGE_LOOP('',(#6854));
#2193=EDGE_LOOP('',(#6855));
#2194=EDGE_LOOP('',(#6856));
#2784=LINE('',#14787,#3267);
#2785=LINE('',#14793,#3268);
#3267=VECTOR('',#11753,0.505);
#3268=VECTOR('',#11760,0.7);
#3747=CIRCLE('',#9670,0.505);
#3748=CIRCLE('',#9671,0.505);
#3749=CIRCLE('',#9673,0.7);
#3750=CIRCLE('',#9674,0.7);
#4351=VERTEX_POINT('',#14784);
#4352=VERTEX_POINT('',#14786);
#4353=VERTEX_POINT('',#14790);
#4354=VERTEX_POINT('',#14792);
#5233=EDGE_CURVE('',#4351,#4351,#3747,.T.);
#5234=EDGE_CURVE('',#4351,#4352,#2784,.T.);
#5235=EDGE_CURVE('',#4352,#4352,#3748,.T.);
#5236=EDGE_CURVE('',#4353,#4353,#3749,.T.);
#5237=EDGE_CURVE('',#4353,#4354,#2785,.T.);
#5238=EDGE_CURVE('',#4354,#4354,#3750,.T.);
#6845=ORIENTED_EDGE('',*,*,#5233,.F.);
#6846=ORIENTED_EDGE('',*,*,#5234,.T.);
#6847=ORIENTED_EDGE('',*,*,#5235,.T.);
#6848=ORIENTED_EDGE('',*,*,#5234,.F.);
#6849=ORIENTED_EDGE('',*,*,#5236,.F.);
#6850=ORIENTED_EDGE('',*,*,#5237,.T.);
#6851=ORIENTED_EDGE('',*,*,#5238,.T.);
#6852=ORIENTED_EDGE('',*,*,#5237,.F.);
#6853=ORIENTED_EDGE('',*,*,#5236,.T.);
#6854=ORIENTED_EDGE('',*,*,#5233,.T.);
#6855=ORIENTED_EDGE('',*,*,#5238,.F.);
#6856=ORIENTED_EDGE('',*,*,#5235,.F.);
#7779=CYLINDRICAL_SURFACE('',#9669,0.505);
#7780=CYLINDRICAL_SURFACE('',#9672,0.7);
#8137=ADVANCED_FACE('',(#1534),#7779,.F.);
#8138=ADVANCED_FACE('',(#1535),#7780,.T.);
#8139=ADVANCED_FACE('',(#1536,#907),#1131,.T.);
#8140=ADVANCED_FACE('',(#1537,#908),#1132,.F.);
#8393=CLOSED_SHELL('',(#8137,#8138,#8139,#8140));
#9668=AXIS2_PLACEMENT_3D('',#14782,#11747,#11748);
#9669=AXIS2_PLACEMENT_3D('',#14783,#11749,#11750);
#9670=AXIS2_PLACEMENT_3D('',#14785,#11751,#11752);
#9671=AXIS2_PLACEMENT_3D('',#14788,#11754,#11755);
#9672=AXIS2_PLACEMENT_3D('',#14789,#11756,#11757);
#9673=AXIS2_PLACEMENT_3D('',#14791,#11758,#11759);
#9674=AXIS2_PLACEMENT_3D('',#14794,#11761,#11762);
#9675=AXIS2_PLACEMENT_3D('',#14795,#11763,#11764);
#9676=AXIS2_PLACEMENT_3D('',#14796,#11765,#11766);
#11747=DIRECTION('axis',(0.,0.,1.));
#11748=DIRECTION('refdir',(1.,0.,0.));
#11749=DIRECTION('center_axis',(0.,1.,0.));
#11750=DIRECTION('ref_axis',(1.,0.,0.));
#11751=DIRECTION('center_axis',(0.,-1.,0.));
#11752=DIRECTION('ref_axis',(1.,0.,0.));
#11753=DIRECTION('',(0.,-1.,0.));
#11754=DIRECTION('center_axis',(0.,-1.,0.));
#11755=DIRECTION('ref_axis',(1.,0.,0.));
#11756=DIRECTION('center_axis',(0.,1.,0.));
#11757=DIRECTION('ref_axis',(1.,0.,0.));
#11758=DIRECTION('center_axis',(0.,1.,0.));
#11759=DIRECTION('ref_axis',(1.,0.,0.));
#11760=DIRECTION('',(0.,-1.,0.));
#11761=DIRECTION('center_axis',(0.,1.,0.));
#11762=DIRECTION('ref_axis',(1.,0.,0.));
#11763=DIRECTION('center_axis',(0.,1.,0.));
#11764=DIRECTION('ref_axis',(1.,0.,0.));
#11765=DIRECTION('center_axis',(0.,1.,0.));
#11766=DIRECTION('ref_axis',(1.,0.,0.));
#14782=CARTESIAN_POINT('',(0.,0.,0.));
#14783=CARTESIAN_POINT('Origin',(0.,15.45,3.5));
#14784=CARTESIAN_POINT('',(-0.505,15.9,3.5));
#14785=CARTESIAN_POINT('Origin',(0.,15.9,3.5));
#14786=CARTESIAN_POINT('',(-0.505,15.45,3.5));
#14787=CARTESIAN_POINT('',(-0.505,15.45,3.5));
#14788=CARTESIAN_POINT('Origin',(0.,15.45,3.5));
#14789=CARTESIAN_POINT('Origin',(0.,15.45,3.5));
#14790=CARTESIAN_POINT('',(-0.7,15.9,3.5));
#14791=CARTESIAN_POINT('Origin',(0.,15.9,3.5));
#14792=CARTESIAN_POINT('',(-0.7,15.45,3.5));
#14793=CARTESIAN_POINT('',(-0.7,15.45,3.5));
#14794=CARTESIAN_POINT('Origin',(0.,15.45,3.5));
#14795=CARTESIAN_POINT('Origin',(0.,15.9,3.5));
#14796=CARTESIAN_POINT('Origin',(0.,15.45,3.5));
#16174=UNCERTAINTY_MEASURE_WITH_UNIT(LENGTH_MEASURE(0.001),#16282,
'DISTANCE_ACCURACY_VALUE',
'Maximum model space distance between geometric entities at asserted c
onnectivities');
#16212=UNCERTAINTY_MEASURE_WITH_UNIT(LENGTH_MEASURE(0.001),#16282,
'DISTANCE_ACCURACY_VALUE',
'Maximum model space distance between geometric entities at asserted c
onnectivities');
#16243=(
GEOMETRIC_REPRESENTATION_CONTEXT(3)
GLOBAL_UNCERTAINTY_ASSIGNED_CONTEXT((#16174))
GLOBAL_UNIT_ASSIGNED_CONTEXT((#16282,#16284,#16285))
REPRESENTATION_CONTEXT('','3D')
);
#16281=(
GEOMETRIC_REPRESENTATION_CONTEXT(3)
GLOBAL_UNCERTAINTY_ASSIGNED_CONTEXT((#16212))
GLOBAL_UNIT_ASSIGNED_CONTEXT((#16282,#16284,#16285))
REPRESENTATION_CONTEXT('','3D')
);
#16282=(
LENGTH_UNIT()
NAMED_UNIT(*)
SI_UNIT(.CENTI.,.METRE.)
);
#16284=(
NAMED_UNIT(*)
PLANE_ANGLE_UNIT()
SI_UNIT($,.RADIAN.)
);
#16285=(
NAMED_UNIT(*)
SI_UNIT($,.STERADIAN.)
SOLID_ANGLE_UNIT()
);
#16316=SHAPE_DEFINITION_REPRESENTATION(#16410,#16549);
#16410=PRODUCT_DEFINITION_SHAPE('',$,#16618);
#16549=SHAPE_REPRESENTATION('',(#9668),#16243);
#16587=PRODUCT_DEFINITION_CONTEXT('part definition',#16793,'design');
#16618=PRODUCT_DEFINITION('Inner race spacer (3)','Inner race spacer (3)',
#16686,#16587);
#16686=PRODUCT_DEFINITION_FORMATION('',$,#16825);
#16793=APPLICATION_CONTEXT(
'Core Data for Automotive Mechanical Design Process');
#16794=PRODUCT_CONTEXT('part definition',#16793,'mechanical');
#16825=PRODUCT('Inner race spacer (3)','Inner race spacer (3)',
'Inner race spacer (3)',(#16794));
#16926=COLOUR_RGB('Grey',0.48,0.52,0.57);
#16927=FILL_AREA_STYLE_COLOUR('',#16926);
#16928=FILL_AREA_STYLE('',(#16927));
#16929=SURFACE_STYLE_FILL_AREA(#16928);
#16930=SURFACE_SIDE_STYLE('',(#16929));
#16931=SURFACE_STYLE_USAGE(.BOTH.,#16930);
#16932=PRESENTATION_STYLE_ASSIGNMENT((#16931));
ENDSEC;
END-ISO-10303-21;
